ISO-10303-21;
HEADER;
/* Generated by software containing ST-Developer
 * from STEP Tools, Inc. (www.steptools.com) 
 */

FILE_DESCRIPTION(
/* description */ ('Hook toggle clamp'),
/* implementation_level */ '2;1');

FILE_NAME(
/* name */ 'Flat Washer - M8.step',
/* time_stamp */ '2026-10-27T21:56:56-07:00',
/* author */ (''),
/* organization */ (''),
/* preprocessor_version */ 'ST-DEVELOPER v20.2',
/* originating_system */ 'Autodesk Translation Framework v15.17.0.0',
/* authorisation */ '');

FILE_SCHEMA (('AUTOMOTIVE_DESIGN { 1 0 10303 214 3 1 1 }'));
ENDSEC;

DATA;
#10=MECHANICAL_DESIGN_GEOMETRIC_PRESENTATION_REPRESENTATION('',(#204),#5458);
#170=SHAPE_REPRESENTATION_RELATIONSHIP('SRR','None',#5554,#187);
#187=ADVANCED_BREP_SHAPE_REPRESENTATION('',(#220),#5456);
#204=STYLED_ITEM('',(#5724),#220);
#220=MANIFOLD_SOLID_BREP('Body1',#2986);
#274=FACE_BOUND('',#779,.T.);
#275=FACE_BOUND('',#781,.T.);
#383=PLANE('',#3480);
#384=PLANE('',#3481);
#551=FACE_OUTER_BOUND('',#776,.T.);
#552=FACE_OUTER_BOUND('',#777,.T.);
#553=FACE_OUTER_BOUND('',#778,.T.);
#554=FACE_OUTER_BOUND('',#780,.T.);
#776=EDGE_LOOP('',(#2687,#2688,#2689,#2690));
#777=EDGE_LOOP('',(#2691,#2692,#2693,#2694));
#778=EDGE_LOOP('',(#2695));
#779=EDGE_LOOP('',(#2696));
#780=EDGE_LOOP('',(#2697));
#781=EDGE_LOOP('',(#2698));
#1021=LINE('',#5313,#1258);
#1022=LINE('',#5319,#1259);
#1258=VECTOR('',#4337,0.42);
#1259=VECTOR('',#4344,0.8);
#1374=CIRCLE('',#3475,0.42);
#1375=CIRCLE('',#3476,0.42);
#1376=CIRCLE('',#3478,0.8);
#1377=CIRCLE('',#3479,0.8);
#1607=VERTEX_POINT('',#5310);
#1608=VERTEX_POINT('',#5312);
#1609=VERTEX_POINT('',#5316);
#1610=VERTEX_POINT('',#5318);
#1970=EDGE_CURVE('',#1607,#1607,#1374,.T.);
#1971=EDGE_CURVE('',#1607,#1608,#1021,.T.);
#1972=EDGE_CURVE('',#1608,#1608,#1375,.T.);
#1973=EDGE_CURVE('',#1609,#1609,#1376,.T.);
#1974=EDGE_CURVE('',#1609,#1610,#1022,.T.);
#1975=EDGE_CURVE('',#1610,#1610,#1377,.T.);
#2687=ORIENTED_EDGE('',*,*,#1970,.F.);
#2688=ORIENTED_EDGE('',*,*,#1971,.T.);
#2689=ORIENTED_EDGE('',*,*,#1972,.T.);
#2690=ORIENTED_EDGE('',*,*,#1971,.F.);
#2691=ORIENTED_EDGE('',*,*,#1973,.F.);
#2692=ORIENTED_EDGE('',*,*,#1974,.T.);
#2693=ORIENTED_EDGE('',*,*,#1975,.T.);
#2694=ORIENTED_EDGE('',*,*,#1974,.F.);
#2695=ORIENTED_EDGE('',*,*,#1973,.T.);
#2696=ORIENTED_EDGE('',*,*,#1970,.T.);
#2697=ORIENTED_EDGE('',*,*,#1975,.F.);
#2698=ORIENTED_EDGE('',*,*,#1972,.F.);
#2794=CYLINDRICAL_SURFACE('',#3474,0.42);
#2795=CYLINDRICAL_SURFACE('',#3477,0.8);
#2955=ADVANCED_FACE('',(#551),#2794,.F.);
#2956=ADVANCED_FACE('',(#552),#2795,.T.);
#2957=ADVANCED_FACE('',(#553,#274),#383,.T.);
#2958=ADVANCED_FACE('',(#554,#275),#384,.F.);
#2986=CLOSED_SHELL('',(#2955,#2956,#2957,#2958));
#3473=AXIS2_PLACEMENT_3D('',#5308,#4331,#4332);
#3474=AXIS2_PLACEMENT_3D('',#5309,#4333,#4334);
#3475=AXIS2_PLACEMENT_3D('',#5311,#4335,#4336);
#3476=AXIS2_PLACEMENT_3D('',#5314,#4338,#4339);
#3477=AXIS2_PLACEMENT_3D('',#5315,#4340,#4341);
#3478=AXIS2_PLACEMENT_3D('',#5317,#4342,#4343);
#3479=AXIS2_PLACEMENT_3D('',#5320,#4345,#4346);
#3480=AXIS2_PLACEMENT_3D('',#5321,#4347,#4348);
#3481=AXIS2_PLACEMENT_3D('',#5322,#4349,#4350);
#4331=DIRECTION('axis',(0.,0.,1.));
#4332=DIRECTION('refdir',(1.,0.,0.));
#4333=DIRECTION('center_axis',(0.,1.,0.));
#4334=DIRECTION('ref_axis',(1.,0.,0.));
#4335=DIRECTION('center_axis',(0.,-1.,0.));
#4336=DIRECTION('ref_axis',(1.,0.,0.));
#4337=DIRECTION('',(0.,-1.,0.));
#4338=DIRECTION('center_axis',(0.,-1.,0.));
#4339=DIRECTION('ref_axis',(1.,0.,0.));
#4340=DIRECTION('center_axis',(0.,1.,0.));
#4341=DIRECTION('ref_axis',(1.,0.,0.));
#4342=DIRECTION('center_axis',(0.,1.,0.));
#4343=DIRECTION('ref_axis',(1.,0.,0.));
#4344=DIRECTION('',(0.,-1.,0.));
#4345=DIRECTION('center_axis',(0.,1.,0.));
#4346=DIRECTION('ref_axis',(1.,0.,0.));
#4347=DIRECTION('center_axis',(0.,1.,0.));
#4348=DIRECTION('ref_axis',(1.,0.,0.));
#4349=DIRECTION('center_axis',(0.,1.,0.));
#4350=DIRECTION('ref_axis',(1.,0.,0.));
#5308=CARTESIAN_POINT('',(0.,0.,0.));
#5309=CARTESIAN_POINT('Origin',(0.,0.,0.));
#5310=CARTESIAN_POINT('',(-0.42,0.16,5.14351655641888E-17));
#5311=CARTESIAN_POINT('Origin',(0.,0.16,0.));
#5312=CARTESIAN_POINT('',(-0.42,0.,5.14351655641888E-17));
#5313=CARTESIAN_POINT('',(-0.42,0.,5.14351655641888E-17));
#5314=CARTESIAN_POINT('Origin',(0.,0.,0.));
#5315=CARTESIAN_POINT('Origin',(0.,0.,0.));
#5316=CARTESIAN_POINT('',(-0.8,0.16,9.79717439317883E-17));
#5317=CARTESIAN_POINT('Origin',(0.,0.16,0.));
#5318=CARTESIAN_POINT('',(-0.8,0.,9.79717439317883E-17));
#5319=CARTESIAN_POINT('',(-0.8,0.,9.79717439317883E-17));
#5320=CARTESIAN_POINT('Origin',(0.,0.,0.));
#5321=CARTESIAN_POINT('Origin',(0.,0.16,0.));
#5322=CARTESIAN_POINT('Origin',(0.,0.,0.));
#5433=UNCERTAINTY_MEASURE_WITH_UNIT(LENGTH_MEASURE(0.001),#5459,
'DISTANCE_ACCURACY_VALUE',
'Maximum model space distance between geometric entities at asserted c
onnectivities');
#5435=UNCERTAINTY_MEASURE_WITH_UNIT(LENGTH_MEASURE(0.001),#5459,
'DISTANCE_ACCURACY_VALUE',
'Maximum model space distance between geometric entities at asserted c
onnectivities');
#5456=(
GEOMETRIC_REPRESENTATION_CONTEXT(3)
GLOBAL_UNCERTAINTY_ASSIGNED_CONTEXT((#5433))
GLOBAL_UNIT_ASSIGNED_CONTEXT((#5459,#5461,#5462))
REPRESENTATION_CONTEXT('','3D')
);
#5458=(
GEOMETRIC_REPRESENTATION_CONTEXT(3)
GLOBAL_UNCERTAINTY_ASSIGNED_CONTEXT((#5435))
GLOBAL_UNIT_ASSIGNED_CONTEXT((#5459,#5461,#5462))
REPRESENTATION_CONTEXT('','3D')
);
#5459=(
LENGTH_UNIT()
NAMED_UNIT(*)
SI_UNIT(.CENTI.,.METRE.)
);
#5461=(
NAMED_UNIT(*)
PLANE_ANGLE_UNIT()
SI_UNIT($,.RADIAN.)
);
#5462=(
NAMED_UNIT(*)
SI_UNIT($,.STERADIAN.)
SOLID_ANGLE_UNIT()
);
#5483=SHAPE_DEFINITION_REPRESENTATION(#5519,#5554);
#5519=PRODUCT_DEFINITION_SHAPE('',$,#5577);
#5554=SHAPE_REPRESENTATION('',(#3473),#5456);
#5556=PRODUCT_DEFINITION_CONTEXT('part definition',#5624,'design');
#5577=PRODUCT_DEFINITION('Flat Washer - M8','Flat Washer - M8',#5599,#5556);
#5599=PRODUCT_DEFINITION_FORMATION('',$,#5646);
#5624=APPLICATION_CONTEXT(
'Core Data for Automotive Mechanical Design Process');
#5625=PRODUCT_CONTEXT('part definition',#5624,'mechanical');
#5646=PRODUCT('Flat Washer - M8','Flat Washer - M8','Flat Washer - M8',
(#5625));
#5718=COLOUR_RGB('Black',0.12,0.14,0.17);
#5719=FILL_AREA_STYLE_COLOUR('',#5718);
#5720=FILL_AREA_STYLE('',(#5719));
#5721=SURFACE_STYLE_FILL_AREA(#5720);
#5722=SURFACE_SIDE_STYLE('',(#5721));
#5723=SURFACE_STYLE_USAGE(.BOTH.,#5722);
#5724=PRESENTATION_STYLE_ASSIGNMENT((#5723));
ENDSEC;
END-ISO-10303-21;
